ISO-10303-21;
HEADER;
/* Generated by software containing ST-Developer
 * from STEP Tools, Inc. (www.steptools.com) 
 */

FILE_DESCRIPTION(
/* description */ ('Lifting hook block with sheave'),
/* implementation_level */ '2;1');

FILE_NAME(
/* name */ 'Outer inner-race spacer (1).step',
/* time_stamp */ '2026-10-28T03:23:54-07:00',
/* author */ (''),
/* organization */ (''),
/* preprocessor_version */ 'ST-DEVELOPER v20.2',
/* originating_system */ 'Autodesk Translation Framework v15.17.0.0',
/* authorisation */ '');

FILE_SCHEMA (('AUTOMOTIVE_DESIGN { 1 0 10303 214 3 1 1 }'));
ENDSEC;

DATA;
#10=MECHANICAL_DESIGN_GEOMETRIC_PRESENTATION_REPRESENTATION('',(#358),#9391);
#298=SHAPE_REPRESENTATION_RELATIONSHIP('SRR','None',#9529,#328);
#328=ADVANCED_BREP_SHAPE_REPRESENTATION('',(#396),#9364);
#358=STYLED_ITEM('',(#9745),#396);
#396=MANIFOLD_SOLID_BREP('Body1',#4894);
#530=LINE('',#7979,#818);
#531=LINE('',#7985,#819);
#818=VECTOR('',#6399,1.005);
#819=VECTOR('',#6406,1.4);
#1038=CYLINDRICAL_SURFACE('',#5439,1.005);
#1039=CYLINDRICAL_SURFACE('',#5442,1.4);
#1149=FACE_BOUND('',#1634,.T.);
#1150=FACE_BOUND('',#1636,.T.);
#1300=FACE_OUTER_BOUND('',#1631,.T.);
#1301=FACE_OUTER_BOUND('',#1632,.T.);
#1302=FACE_OUTER_BOUND('',#1633,.T.);
#1303=FACE_OUTER_BOUND('',#1635,.T.);
#1631=EDGE_LOOP('',(#3626,#3627,#3628,#3629));
#1632=EDGE_LOOP('',(#3630,#3631,#3632,#3633));
#1633=EDGE_LOOP('',(#3634));
#1634=EDGE_LOOP('',(#3635));
#1635=EDGE_LOOP('',(#3636));
#1636=EDGE_LOOP('',(#3637));
#2007=CIRCLE('',#5440,1.005);
#2008=CIRCLE('',#5441,1.005);
#2009=CIRCLE('',#5443,1.4);
#2010=CIRCLE('',#5444,1.4);
#2340=VERTEX_POINT('',#7976);
#2341=VERTEX_POINT('',#7978);
#2342=VERTEX_POINT('',#7982);
#2343=VERTEX_POINT('',#7984);
#2817=EDGE_CURVE('',#2340,#2340,#2007,.T.);
#2818=EDGE_CURVE('',#2340,#2341,#530,.T.);
#2819=EDGE_CURVE('',#2341,#2341,#2008,.T.);
#2820=EDGE_CURVE('',#2342,#2342,#2009,.T.);
#2821=EDGE_CURVE('',#2342,#2343,#531,.T.);
#2822=EDGE_CURVE('',#2343,#2343,#2010,.T.);
#3626=ORIENTED_EDGE('',*,*,#2817,.F.);
#3627=ORIENTED_EDGE('',*,*,#2818,.T.);
#3628=ORIENTED_EDGE('',*,*,#2819,.T.);
#3629=ORIENTED_EDGE('',*,*,#2818,.F.);
#3630=ORIENTED_EDGE('',*,*,#2820,.F.);
#3631=ORIENTED_EDGE('',*,*,#2821,.T.);
#3632=ORIENTED_EDGE('',*,*,#2822,.T.);
#3633=ORIENTED_EDGE('',*,*,#2821,.F.);
#3634=ORIENTED_EDGE('',*,*,#2820,.T.);
#3635=ORIENTED_EDGE('',*,*,#2817,.T.);
#3636=ORIENTED_EDGE('',*,*,#2822,.F.);
#3637=ORIENTED_EDGE('',*,*,#2819,.F.);
#4492=PLANE('',#5445);
#4493=PLANE('',#5446);
#4676=ADVANCED_FACE('',(#1300),#1038,.F.);
#4677=ADVANCED_FACE('',(#1301),#1039,.T.);
#4678=ADVANCED_FACE('',(#1302,#1149),#4492,.T.);
#4679=ADVANCED_FACE('',(#1303,#1150),#4493,.F.);
#4894=CLOSED_SHELL('',(#4676,#4677,#4678,#4679));
#5438=AXIS2_PLACEMENT_3D('',#7974,#6393,#6394);
#5439=AXIS2_PLACEMENT_3D('',#7975,#6395,#6396);
#5440=AXIS2_PLACEMENT_3D('',#7977,#6397,#6398);
#5441=AXIS2_PLACEMENT_3D('',#7980,#6400,#6401);
#5442=AXIS2_PLACEMENT_3D('',#7981,#6402,#6403);
#5443=AXIS2_PLACEMENT_3D('',#7983,#6404,#6405);
#5444=AXIS2_PLACEMENT_3D('',#7986,#6407,#6408);
#5445=AXIS2_PLACEMENT_3D('',#7987,#6409,#6410);
#5446=AXIS2_PLACEMENT_3D('',#7988,#6411,#6412);
#6393=DIRECTION('axis',(0.,0.,1.));
#6394=DIRECTION('refdir',(1.,0.,0.));
#6395=DIRECTION('center_axis',(0.,1.,0.));
#6396=DIRECTION('ref_axis',(1.,0.,0.));
#6397=DIRECTION('center_axis',(0.,-1.,0.));
#6398=DIRECTION('ref_axis',(1.,0.,0.));
#6399=DIRECTION('',(0.,-1.,0.));
#6400=DIRECTION('center_axis',(0.,-1.,0.));
#6401=DIRECTION('ref_axis',(1.,0.,0.));
#6402=DIRECTION('center_axis',(0.,1.,0.));
#6403=DIRECTION('ref_axis',(1.,0.,0.));
#6404=DIRECTION('center_axis',(0.,1.,0.));
#6405=DIRECTION('ref_axis',(1.,0.,0.));
#6406=DIRECTION('',(0.,-1.,0.));
#6407=DIRECTION('center_axis',(0.,1.,0.));
#6408=DIRECTION('ref_axis',(1.,0.,0.));
#6409=DIRECTION('center_axis',(0.,1.,0.));
#6410=DIRECTION('ref_axis',(1.,0.,0.));
#6411=DIRECTION('center_axis',(0.,1.,0.));
#6412=DIRECTION('ref_axis',(1.,0.,0.));
#7974=CARTESIAN_POINT('',(0.,0.,0.));
#7975=CARTESIAN_POINT('Origin',(0.,1.7,12.));
#7976=CARTESIAN_POINT('',(-1.005,2.5,12.));
#7977=CARTESIAN_POINT('Origin',(0.,2.5,12.));
#7978=CARTESIAN_POINT('',(-1.005,1.7,12.));
#7979=CARTESIAN_POINT('',(-1.005,1.7,12.));
#7980=CARTESIAN_POINT('Origin',(0.,1.7,12.));
#7981=CARTESIAN_POINT('Origin',(0.,1.7,12.));
#7982=CARTESIAN_POINT('',(-1.4,2.5,12.));
#7983=CARTESIAN_POINT('Origin',(0.,2.5,12.));
#7984=CARTESIAN_POINT('',(-1.4,1.7,12.));
#7985=CARTESIAN_POINT('',(-1.4,1.7,12.));
#7986=CARTESIAN_POINT('Origin',(0.,1.7,12.));
#7987=CARTESIAN_POINT('Origin',(0.,2.5,12.));
#7988=CARTESIAN_POINT('Origin',(0.,1.7,12.));
#9327=UNCERTAINTY_MEASURE_WITH_UNIT(LENGTH_MEASURE(0.001),#9392,
'DISTANCE_ACCURACY_VALUE',
'Maximum model space distance between geometric entities at asserted c
onnectivities');
#9354=UNCERTAINTY_MEASURE_WITH_UNIT(LENGTH_MEASURE(0.001),#9392,
'DISTANCE_ACCURACY_VALUE',
'Maximum model space distance between geometric entities at asserted c
onnectivities');
#9364=(
GEOMETRIC_REPRESENTATION_CONTEXT(3)
GLOBAL_UNCERTAINTY_ASSIGNED_CONTEXT((#9327))
GLOBAL_UNIT_ASSIGNED_CONTEXT((#9392,#9394,#9395))
REPRESENTATION_CONTEXT('','3D')
);
#9391=(
GEOMETRIC_REPRESENTATION_CONTEXT(3)
GLOBAL_UNCERTAINTY_ASSIGNED_CONTEXT((#9354))
GLOBAL_UNIT_ASSIGNED_CONTEXT((#9392,#9394,#9395))
REPRESENTATION_CONTEXT('','3D')
);
#9392=(
LENGTH_UNIT()
NAMED_UNIT(*)
SI_UNIT(.CENTI.,.METRE.)
);
#9394=(
NAMED_UNIT(*)
PLANE_ANGLE_UNIT()
SI_UNIT($,.RADIAN.)
);
#9395=(
NAMED_UNIT(*)
SI_UNIT($,.STERADIAN.)
SOLID_ANGLE_UNIT()
);
#9405=SHAPE_DEFINITION_REPRESENTATION(#9441,#9529);
#9441=PRODUCT_DEFINITION_SHAPE('',$,#9566);
#9529=SHAPE_REPRESENTATION('',(#5438),#9364);
#9556=PRODUCT_DEFINITION_CONTEXT('part definition',#9666,'design');
#9566=PRODUCT_DEFINITION('Outer inner-race spacer (1)',
'Outer inner-race spacer (1)',#9602,#9556);
#9602=PRODUCT_DEFINITION_FORMATION('',$,#9677);
#9666=APPLICATION_CONTEXT(
'Core Data for Automotive Mechanical Design Process');
#9667=PRODUCT_CONTEXT('part definition',#9666,'mechanical');
#9677=PRODUCT('Outer inner-race spacer (1)','Outer inner-race spacer (1)',
'Outer inner-race spacer (1)',(#9667));
#9739=COLOUR_RGB('Light Blue',0.38,0.62,0.78);
#9740=FILL_AREA_STYLE_COLOUR('',#9739);
#9741=FILL_AREA_STYLE('',(#9740));
#9742=SURFACE_STYLE_FILL_AREA(#9741);
#9743=SURFACE_SIDE_STYLE('',(#9742));
#9744=SURFACE_STYLE_USAGE(.BOTH.,#9743);
#9745=PRESENTATION_STYLE_ASSIGNMENT((#9744));
ENDSEC;
END-ISO-10303-21;
